ISO-10303-21;
HEADER;
/* Generated by software containing ST-Developer
 * from STEP Tools, Inc. (www.steptools.com) 
 */

FILE_DESCRIPTION(
/* description */ ('Flywheel Crank-Slider'),
/* implementation_level */ '2;1');

FILE_NAME(
/* name */ 'M4x10 Cap Screw.step',
/* time_stamp */ '2026-10-28T03:23:13-07:00',
/* author */ (''),
/* organization */ (''),
/* preprocessor_version */ 'ST-DEVELOPER v20.2',
/* originating_system */ 'Autodesk Translation Framework v15.17.0.0',
/* authorisation */ '');

FILE_SCHEMA (('AUTOMOTIVE_DESIGN { 1 0 10303 214 3 1 1 }'));
ENDSEC;

DATA;
#10=MECHANICAL_DESIGN_GEOMETRIC_PRESENTATION_REPRESENTATION('',(#728),#17322);
#533=ORIENTED_CLOSED_SHELL('',*,#9110,.F.);
#556=CONICAL_SURFACE('',#10724,0.325,0.785398163397448);
#557=CONICAL_SURFACE('',#10728,0.335,0.785398163397448);
#558=CONICAL_SURFACE('',#10732,0.21,0.463647609000806);
#563=BREP_WITH_VOIDS('Body1',#9111,(#533));
#615=SHAPE_REPRESENTATION_RELATIONSHIP('SRR','None',#17617,#667);
#667=ADVANCED_BREP_SHAPE_REPRESENTATION('',(#563),#17321);
#728=STYLED_ITEM('',(#17938),#563);
#1010=FACE_BOUND('',#2613,.T.);
#1309=PLANE('',#10712);
#1310=PLANE('',#10713);
#1311=PLANE('',#10714);
#1312=PLANE('',#10715);
#1313=PLANE('',#10716);
#1314=PLANE('',#10717);
#1315=PLANE('',#10718);
#1316=PLANE('',#10719);
#1317=PLANE('',#10720);
#1318=PLANE('',#10722);
#1319=PLANE('',#10730);
#1839=FACE_OUTER_BOUND('',#2599,.T.);
#1840=FACE_OUTER_BOUND('',#2600,.T.);
#1841=FACE_OUTER_BOUND('',#2601,.T.);
#1842=FACE_OUTER_BOUND('',#2602,.T.);
#1843=FACE_OUTER_BOUND('',#2603,.T.);
#1844=FACE_OUTER_BOUND('',#2604,.T.);
#1845=FACE_OUTER_BOUND('',#2605,.T.);
#1846=FACE_OUTER_BOUND('',#2606,.T.);
#1847=FACE_OUTER_BOUND('',#2607,.T.);
#1848=FACE_OUTER_BOUND('',#2608,.T.);
#1849=FACE_OUTER_BOUND('',#2609,.T.);
#1850=FACE_OUTER_BOUND('',#2610,.T.);
#1851=FACE_OUTER_BOUND('',#2611,.T.);
#1852=FACE_OUTER_BOUND('',#2612,.T.);
#1853=FACE_OUTER_BOUND('',#2614,.T.);
#1854=FACE_OUTER_BOUND('',#2615,.T.);
#2599=EDGE_LOOP('',(#8270,#8271,#8272,#8273));
#2600=EDGE_LOOP('',(#8274,#8275,#8276,#8277));
#2601=EDGE_LOOP('',(#8278,#8279,#8280,#8281));
#2602=EDGE_LOOP('',(#8282,#8283,#8284,#8285));
#2603=EDGE_LOOP('',(#8286,#8287,#8288,#8289));
#2604=EDGE_LOOP('',(#8290,#8291,#8292,#8293));
#2605=EDGE_LOOP('',(#8294,#8295,#8296,#8297,#8298,#8299));
#2606=EDGE_LOOP('',(#8300,#8301,#8302,#8303,#8304,#8305));
#2607=EDGE_LOOP('',(#8306));
#2608=EDGE_LOOP('',(#8307));
#2609=EDGE_LOOP('',(#8308,#8309,#8310,#8311));
#2610=EDGE_LOOP('',(#8312,#8313,#8314,#8315));
#2611=EDGE_LOOP('',(#8316,#8317,#8318,#8319));
#2612=EDGE_LOOP('',(#8320));
#2613=EDGE_LOOP('',(#8321));
#2614=EDGE_LOOP('',(#8322,#8323,#8324,#8325));
#2615=EDGE_LOOP('',(#8326,#8327,#8328,#8329));
#3204=LINE('',#17044,#3815);
#3205=LINE('',#17046,#3816);
#3206=LINE('',#17048,#3817);
#3207=LINE('',#17049,#3818);
#3208=LINE('',#17052,#3819);
#3209=LINE('',#17054,#3820);
#3210=LINE('',#17055,#3821);
#3211=LINE('',#17058,#3822);
#3212=LINE('',#17060,#3823);
#3213=LINE('',#17061,#3824);
#3214=LINE('',#17064,#3825);
#3215=LINE('',#17066,#3826);
#3216=LINE('',#17067,#3827);
#3217=LINE('',#17070,#3828);
#3218=LINE('',#17072,#3829);
#3219=LINE('',#17073,#3830);
#3220=LINE('',#17075,#3831);
#3221=LINE('',#17076,#3832);
#3222=LINE('',#17088,#3833);
#3223=LINE('',#17092,#3834);
#3224=LINE('',#17096,#3835);
#3225=LINE('',#17103,#3836);
#3226=LINE('',#17105,#3837);
#3815=VECTOR('',#13474,1.);
#3816=VECTOR('',#13475,1.);
#3817=VECTOR('',#13476,1.);
#3818=VECTOR('',#13477,1.);
#3819=VECTOR('',#13480,1.);
#3820=VECTOR('',#13481,1.);
#3821=VECTOR('',#13482,1.);
#3822=VECTOR('',#13485,1.);
#3823=VECTOR('',#13486,1.);
#3824=VECTOR('',#13487,1.);
#3825=VECTOR('',#13490,1.);
#3826=VECTOR('',#13491,1.);
#3827=VECTOR('',#13492,1.);
#3828=VECTOR('',#13495,1.);
#3829=VECTOR('',#13496,1.);
#3830=VECTOR('',#13497,1.);
#3831=VECTOR('',#13500,1.);
#3832=VECTOR('',#13501,1.);
#3833=VECTOR('',#13518,0.325);
#3834=VECTOR('',#13523,0.35);
#3835=VECTOR('',#13528,0.335);
#3836=VECTOR('',#13537,0.21);
#3837=VECTOR('',#13540,0.2);
#4270=CIRCLE('',#10721,0.1954);
#4271=CIRCLE('',#10723,0.3);
#4272=CIRCLE('',#10725,0.35);
#4273=CIRCLE('',#10727,0.35);
#4274=CIRCLE('',#10729,0.32);
#4275=CIRCLE('',#10731,0.22);
#4276=CIRCLE('',#10733,0.1954);
#4999=VERTEX_POINT('',#17042);
#5000=VERTEX_POINT('',#17043);
#5001=VERTEX_POINT('',#17045);
#5002=VERTEX_POINT('',#17047);
#5003=VERTEX_POINT('',#17051);
#5004=VERTEX_POINT('',#17053);
#5005=VERTEX_POINT('',#17057);
#5006=VERTEX_POINT('',#17059);
#5007=VERTEX_POINT('',#17063);
#5008=VERTEX_POINT('',#17065);
#5009=VERTEX_POINT('',#17069);
#5010=VERTEX_POINT('',#17071);
#5011=VERTEX_POINT('',#17080);
#5012=VERTEX_POINT('',#17083);
#5013=VERTEX_POINT('',#17086);
#5014=VERTEX_POINT('',#17090);
#5015=VERTEX_POINT('',#17094);
#5016=VERTEX_POINT('',#17098);
#5017=VERTEX_POINT('',#17101);
#6092=EDGE_CURVE('',#4999,#5000,#3204,.T.);
#6093=EDGE_CURVE('',#5000,#5001,#3205,.T.);
#6094=EDGE_CURVE('',#5001,#5002,#3206,.T.);
#6095=EDGE_CURVE('',#4999,#5002,#3207,.T.);
#6096=EDGE_CURVE('',#5000,#5003,#3208,.T.);
#6097=EDGE_CURVE('',#5003,#5004,#3209,.T.);
#6098=EDGE_CURVE('',#5004,#5001,#3210,.T.);
#6099=EDGE_CURVE('',#5003,#5005,#3211,.T.);
#6100=EDGE_CURVE('',#5005,#5006,#3212,.T.);
#6101=EDGE_CURVE('',#5006,#5004,#3213,.T.);
#6102=EDGE_CURVE('',#5005,#5007,#3214,.T.);
#6103=EDGE_CURVE('',#5007,#5008,#3215,.T.);
#6104=EDGE_CURVE('',#5008,#5006,#3216,.T.);
#6105=EDGE_CURVE('',#5007,#5009,#3217,.T.);
#6106=EDGE_CURVE('',#5009,#5010,#3218,.T.);
#6107=EDGE_CURVE('',#5010,#5008,#3219,.T.);
#6108=EDGE_CURVE('',#5009,#4999,#3220,.T.);
#6109=EDGE_CURVE('',#5002,#5010,#3221,.T.);
#6110=EDGE_CURVE('',#5011,#5011,#4270,.T.);
#6111=EDGE_CURVE('',#5012,#5012,#4271,.T.);
#6112=EDGE_CURVE('',#5013,#5013,#4272,.T.);
#6113=EDGE_CURVE('',#5013,#5012,#3222,.T.);
#6114=EDGE_CURVE('',#5014,#5014,#4273,.T.);
#6115=EDGE_CURVE('',#5014,#5013,#3223,.T.);
#6116=EDGE_CURVE('',#5015,#5015,#4274,.T.);
#6117=EDGE_CURVE('',#5015,#5014,#3224,.T.);
#6118=EDGE_CURVE('',#5016,#5016,#4275,.T.);
#6119=EDGE_CURVE('',#5017,#5017,#4276,.F.);
#6120=EDGE_CURVE('',#5017,#5016,#3225,.T.);
#6121=EDGE_CURVE('',#5011,#5017,#3226,.T.);
#8270=ORIENTED_EDGE('',*,*,#6092,.T.);
#8271=ORIENTED_EDGE('',*,*,#6093,.T.);
#8272=ORIENTED_EDGE('',*,*,#6094,.T.);
#8273=ORIENTED_EDGE('',*,*,#6095,.F.);
#8274=ORIENTED_EDGE('',*,*,#6096,.T.);
#8275=ORIENTED_EDGE('',*,*,#6097,.T.);
#8276=ORIENTED_EDGE('',*,*,#6098,.T.);
#8277=ORIENTED_EDGE('',*,*,#6093,.F.);
#8278=ORIENTED_EDGE('',*,*,#6099,.T.);
#8279=ORIENTED_EDGE('',*,*,#6100,.T.);
#8280=ORIENTED_EDGE('',*,*,#6101,.T.);
#8281=ORIENTED_EDGE('',*,*,#6097,.F.);
#8282=ORIENTED_EDGE('',*,*,#6102,.T.);
#8283=ORIENTED_EDGE('',*,*,#6103,.T.);
#8284=ORIENTED_EDGE('',*,*,#6104,.T.);
#8285=ORIENTED_EDGE('',*,*,#6100,.F.);
#8286=ORIENTED_EDGE('',*,*,#6105,.T.);
#8287=ORIENTED_EDGE('',*,*,#6106,.T.);
#8288=ORIENTED_EDGE('',*,*,#6107,.T.);
#8289=ORIENTED_EDGE('',*,*,#6103,.F.);
#8290=ORIENTED_EDGE('',*,*,#6108,.T.);
#8291=ORIENTED_EDGE('',*,*,#6095,.T.);
#8292=ORIENTED_EDGE('',*,*,#6109,.T.);
#8293=ORIENTED_EDGE('',*,*,#6106,.F.);
#8294=ORIENTED_EDGE('',*,*,#6108,.F.);
#8295=ORIENTED_EDGE('',*,*,#6105,.F.);
#8296=ORIENTED_EDGE('',*,*,#6102,.F.);
#8297=ORIENTED_EDGE('',*,*,#6099,.F.);
#8298=ORIENTED_EDGE('',*,*,#6096,.F.);
#8299=ORIENTED_EDGE('',*,*,#6092,.F.);
#8300=ORIENTED_EDGE('',*,*,#6109,.F.);
#8301=ORIENTED_EDGE('',*,*,#6094,.F.);
#8302=ORIENTED_EDGE('',*,*,#6098,.F.);
#8303=ORIENTED_EDGE('',*,*,#6101,.F.);
#8304=ORIENTED_EDGE('',*,*,#6104,.F.);
#8305=ORIENTED_EDGE('',*,*,#6107,.F.);
#8306=ORIENTED_EDGE('',*,*,#6110,.F.);
#8307=ORIENTED_EDGE('',*,*,#6111,.F.);
#8308=ORIENTED_EDGE('',*,*,#6112,.F.);
#8309=ORIENTED_EDGE('',*,*,#6113,.T.);
#8310=ORIENTED_EDGE('',*,*,#6111,.T.);
#8311=ORIENTED_EDGE('',*,*,#6113,.F.);
#8312=ORIENTED_EDGE('',*,*,#6114,.F.);
#8313=ORIENTED_EDGE('',*,*,#6115,.T.);
#8314=ORIENTED_EDGE('',*,*,#6112,.T.);
#8315=ORIENTED_EDGE('',*,*,#6115,.F.);
#8316=ORIENTED_EDGE('',*,*,#6116,.F.);
#8317=ORIENTED_EDGE('',*,*,#6117,.T.);
#8318=ORIENTED_EDGE('',*,*,#6114,.T.);
#8319=ORIENTED_EDGE('',*,*,#6117,.F.);
#8320=ORIENTED_EDGE('',*,*,#6116,.T.);
#8321=ORIENTED_EDGE('',*,*,#6118,.F.);
#8322=ORIENTED_EDGE('',*,*,#6119,.F.);
#8323=ORIENTED_EDGE('',*,*,#6120,.T.);
#8324=ORIENTED_EDGE('',*,*,#6118,.T.);
#8325=ORIENTED_EDGE('',*,*,#6120,.F.);
#8326=ORIENTED_EDGE('',*,*,#6110,.T.);
#8327=ORIENTED_EDGE('',*,*,#6121,.T.);
#8328=ORIENTED_EDGE('',*,*,#6119,.T.);
#8329=ORIENTED_EDGE('',*,*,#6121,.F.);
#8509=CYLINDRICAL_SURFACE('',#10726,0.35);
#8510=CYLINDRICAL_SURFACE('',#10734,0.1954);
#9030=ADVANCED_FACE('',(#1839),#1309,.F.);
#9031=ADVANCED_FACE('',(#1840),#1310,.F.);
#9032=ADVANCED_FACE('',(#1841),#1311,.F.);
#9033=ADVANCED_FACE('',(#1842),#1312,.F.);
#9034=ADVANCED_FACE('',(#1843),#1313,.F.);
#9035=ADVANCED_FACE('',(#1844),#1314,.F.);
#9036=ADVANCED_FACE('',(#1845),#1315,.F.);
#9037=ADVANCED_FACE('',(#1846),#1316,.F.);
#9038=ADVANCED_FACE('',(#1847),#1317,.F.);
#9039=ADVANCED_FACE('',(#1848),#1318,.T.);
#9040=ADVANCED_FACE('',(#1849),#556,.T.);
#9041=ADVANCED_FACE('',(#1850),#8509,.T.);
#9042=ADVANCED_FACE('',(#1851),#557,.T.);
#9043=ADVANCED_FACE('',(#1852,#1010),#1319,.T.);
#9044=ADVANCED_FACE('',(#1853),#558,.T.);
#9045=ADVANCED_FACE('',(#1854),#8510,.T.);
#9110=CLOSED_SHELL('',(#9030,#9031,#9032,#9033,#9034,#9035,#9036,#9037));
#9111=CLOSED_SHELL('',(#9038,#9039,#9040,#9041,#9042,#9043,#9044,#9045));
#10711=AXIS2_PLACEMENT_3D('',#17040,#13470,#13471);
#10712=AXIS2_PLACEMENT_3D('',#17041,#13472,#13473);
#10713=AXIS2_PLACEMENT_3D('',#17050,#13478,#13479);
#10714=AXIS2_PLACEMENT_3D('',#17056,#13483,#13484);
#10715=AXIS2_PLACEMENT_3D('',#17062,#13488,#13489);
#10716=AXIS2_PLACEMENT_3D('',#17068,#13493,#13494);
#10717=AXIS2_PLACEMENT_3D('',#17074,#13498,#13499);
#10718=AXIS2_PLACEMENT_3D('',#17077,#13502,#13503);
#10719=AXIS2_PLACEMENT_3D('',#17078,#13504,#13505);
#10720=AXIS2_PLACEMENT_3D('',#17079,#13506,#13507);
#10721=AXIS2_PLACEMENT_3D('',#17081,#13508,#13509);
#10722=AXIS2_PLACEMENT_3D('',#17082,#13510,#13511);
#10723=AXIS2_PLACEMENT_3D('',#17084,#13512,#13513);
#10724=AXIS2_PLACEMENT_3D('',#17085,#13514,#13515);
#10725=AXIS2_PLACEMENT_3D('',#17087,#13516,#13517);
#10726=AXIS2_PLACEMENT_3D('',#17089,#13519,#13520);
#10727=AXIS2_PLACEMENT_3D('',#17091,#13521,#13522);
#10728=AXIS2_PLACEMENT_3D('',#17093,#13524,#13525);
#10729=AXIS2_PLACEMENT_3D('',#17095,#13526,#13527);
#10730=AXIS2_PLACEMENT_3D('',#17097,#13529,#13530);
#10731=AXIS2_PLACEMENT_3D('',#17099,#13531,#13532);
#10732=AXIS2_PLACEMENT_3D('',#17100,#13533,#13534);
#10733=AXIS2_PLACEMENT_3D('',#17102,#13535,#13536);
#10734=AXIS2_PLACEMENT_3D('',#17104,#13538,#13539);
#13470=DIRECTION('axis',(0.,0.,1.));
#13471=DIRECTION('refdir',(1.,0.,0.));
#13472=DIRECTION('center_axis',(0.866025403784439,0.,-0.5));
#13473=DIRECTION('ref_axis',(0.5,0.,0.866025403784439));
#13474=DIRECTION('',(-0.5,0.,-0.866025403784439));
#13475=DIRECTION('',(0.,-1.,0.));
#13476=DIRECTION('',(0.5,0.,0.866025403784439));
#13477=DIRECTION('',(0.,-1.,0.));
#13478=DIRECTION('center_axis',(1.60246890531964E-16,0.,-1.));
#13479=DIRECTION('ref_axis',(1.,0.,1.60246890531964E-16));
#13480=DIRECTION('',(-1.,0.,-1.60246890531964E-16));
#13481=DIRECTION('',(0.,-1.,0.));
#13482=DIRECTION('',(1.,0.,1.60246890531964E-16));
#13483=DIRECTION('center_axis',(-0.866025403784439,0.,-0.5));
#13484=DIRECTION('ref_axis',(0.5,0.,-0.866025403784439));
#13485=DIRECTION('',(-0.5,0.,0.866025403784439));
#13486=DIRECTION('',(0.,-1.,0.));
#13487=DIRECTION('',(0.5,0.,-0.866025403784439));
#13488=DIRECTION('center_axis',(-0.866025403784439,0.,0.5));
#13489=DIRECTION('ref_axis',(-0.5,0.,-0.866025403784439));
#13490=DIRECTION('',(0.5,0.,0.866025403784439));
#13491=DIRECTION('',(0.,-1.,0.));
#13492=DIRECTION('',(-0.5,0.,-0.866025403784439));
#13493=DIRECTION('center_axis',(-1.60246890531964E-16,0.,1.));
#13494=DIRECTION('ref_axis',(-1.,0.,-1.60246890531964E-16));
#13495=DIRECTION('',(1.,0.,1.60246890531964E-16));
#13496=DIRECTION('',(0.,-1.,0.));
#13497=DIRECTION('',(-1.,0.,-1.60246890531964E-16));
#13498=DIRECTION('center_axis',(0.866025403784439,0.,0.5));
#13499=DIRECTION('ref_axis',(-0.5,0.,0.866025403784439));
#13500=DIRECTION('',(0.5,0.,-0.866025403784439));
#13501=DIRECTION('',(-0.5,0.,0.866025403784439));
#13502=DIRECTION('center_axis',(0.,1.,0.));
#13503=DIRECTION('ref_axis',(1.,0.,0.));
#13504=DIRECTION('center_axis',(0.,-1.,0.));
#13505=DIRECTION('ref_axis',(0.,0.,-1.));
#13506=DIRECTION('center_axis',(0.,1.,0.));
#13507=DIRECTION('ref_axis',(1.,0.,0.));
#13508=DIRECTION('center_axis',(0.,1.,0.));
#13509=DIRECTION('ref_axis',(1.,0.,0.));
#13510=DIRECTION('center_axis',(0.,1.,0.));
#13511=DIRECTION('ref_axis',(0.,0.,1.));
#13512=DIRECTION('center_axis',(0.,-1.,0.));
#13513=DIRECTION('ref_axis',(1.,0.,0.));
#13514=DIRECTION('center_axis',(0.,-1.,0.));
#13515=DIRECTION('ref_axis',(1.,0.,0.));
#13516=DIRECTION('center_axis',(0.,-1.,0.));
#13517=DIRECTION('ref_axis',(1.,0.,0.));
#13518=DIRECTION('',(0.707106781186547,0.707106781186548,8.65956056235493E-17));
#13519=DIRECTION('center_axis',(0.,-1.,0.));
#13520=DIRECTION('ref_axis',(1.,0.,0.));
#13521=DIRECTION('center_axis',(0.,-1.,0.));
#13522=DIRECTION('ref_axis',(1.,0.,0.));
#13523=DIRECTION('',(0.,1.,0.));
#13524=DIRECTION('center_axis',(0.,1.,0.));
#13525=DIRECTION('ref_axis',(1.,0.,0.));
#13526=DIRECTION('center_axis',(0.,-1.,0.));
#13527=DIRECTION('ref_axis',(1.,0.,0.));
#13528=DIRECTION('',(-0.707106781186547,0.707106781186548,-8.65956056235493E-17));
#13529=DIRECTION('center_axis',(0.,-1.,0.));
#13530=DIRECTION('ref_axis',(0.,0.,-1.));
#13531=DIRECTION('center_axis',(0.,-1.,0.));
#13532=DIRECTION('ref_axis',(1.,0.,0.));
#13533=DIRECTION('center_axis',(0.,1.,0.));
#13534=DIRECTION('ref_axis',(1.,0.,0.));
#13535=DIRECTION('center_axis',(0.,1.,0.));
#13536=DIRECTION('ref_axis',(1.,0.,0.));
#13537=DIRECTION('',(-0.447213595499958,0.894427190999916,-5.47678698264203E-17));
#13538=DIRECTION('center_axis',(0.,-1.,0.));
#13539=DIRECTION('ref_axis',(1.,0.,0.));
#13540=DIRECTION('',(0.,1.,0.));
#17040=CARTESIAN_POINT('',(0.,0.,0.));
#17041=CARTESIAN_POINT('Origin',(0.0866025403784439,-0.4,-0.15));
#17042=CARTESIAN_POINT('',(0.173205080756888,-0.4,0.));
#17043=CARTESIAN_POINT('',(0.0866025403784439,-0.4,-0.15));
#17044=CARTESIAN_POINT('',(0.173205080756888,-0.4,0.));
#17045=CARTESIAN_POINT('',(0.0866025403784439,-0.64,-0.15));
#17046=CARTESIAN_POINT('',(0.0866025403784439,-0.4,-0.15));
#17047=CARTESIAN_POINT('',(0.173205080756888,-0.64,0.));
#17048=CARTESIAN_POINT('',(0.173205080756888,-0.64,0.));
#17049=CARTESIAN_POINT('',(0.173205080756888,-0.4,0.));
#17050=CARTESIAN_POINT('Origin',(-0.0866025403784438,-0.4,-0.15));
#17051=CARTESIAN_POINT('',(-0.0866025403784438,-0.4,-0.15));
#17052=CARTESIAN_POINT('',(0.0866025403784439,-0.4,-0.15));
#17053=CARTESIAN_POINT('',(-0.0866025403784438,-0.64,-0.15));
#17054=CARTESIAN_POINT('',(-0.0866025403784438,-0.4,-0.15));
#17055=CARTESIAN_POINT('',(0.0866025403784439,-0.64,-0.15));
#17056=CARTESIAN_POINT('Origin',(-0.173205080756888,-0.4,-2.77555756156289E-17));
#17057=CARTESIAN_POINT('',(-0.173205080756888,-0.4,-2.12115047744981E-17));
#17058=CARTESIAN_POINT('',(-0.0866025403784438,-0.4,-0.15));
#17059=CARTESIAN_POINT('',(-0.173205080756888,-0.64,-2.77555756156289E-17));
#17060=CARTESIAN_POINT('',(-0.173205080756888,-0.4,-2.12115047744981E-17));
#17061=CARTESIAN_POINT('',(-0.0866025403784438,-0.64,-0.15));
#17062=CARTESIAN_POINT('Origin',(-0.0866025403784439,-0.4,0.15));
#17063=CARTESIAN_POINT('',(-0.0866025403784439,-0.4,0.15));
#17064=CARTESIAN_POINT('',(-0.173205080756888,-0.4,-2.12115047744981E-17));
#17065=CARTESIAN_POINT('',(-0.0866025403784439,-0.64,0.15));
#17066=CARTESIAN_POINT('',(-0.0866025403784439,-0.4,0.15));
#17067=CARTESIAN_POINT('',(-0.173205080756888,-0.64,-2.12115047744981E-17));
#17068=CARTESIAN_POINT('Origin',(0.0866025403784439,-0.4,0.15));
#17069=CARTESIAN_POINT('',(0.0866025403784439,-0.4,0.15));
#17070=CARTESIAN_POINT('',(-0.0866025403784439,-0.4,0.15));
#17071=CARTESIAN_POINT('',(0.0866025403784439,-0.64,0.15));
#17072=CARTESIAN_POINT('',(0.0866025403784439,-0.4,0.15));
#17073=CARTESIAN_POINT('',(-0.0866025403784439,-0.64,0.15));
#17074=CARTESIAN_POINT('Origin',(0.173205080756888,-0.4,0.));
#17075=CARTESIAN_POINT('',(0.0866025403784439,-0.4,0.15));
#17076=CARTESIAN_POINT('',(0.0866025403784439,-0.64,0.15));
#17077=CARTESIAN_POINT('Origin',(0.,-0.4,-2.77555756156289E-17));
#17078=CARTESIAN_POINT('Origin',(0.,-0.64,-2.77555756156289E-17));
#17079=CARTESIAN_POINT('Origin',(0.,-1.,0.));
#17080=CARTESIAN_POINT('',(-0.1954,-1.,2.39295984553393E-17));
#17081=CARTESIAN_POINT('Origin',(0.,-1.,0.));
#17082=CARTESIAN_POINT('Origin',(0.3,0.4,0.));
#17083=CARTESIAN_POINT('',(-0.3,0.4,-3.67394039744206E-17));
#17084=CARTESIAN_POINT('Origin',(0.,0.4,0.));
#17085=CARTESIAN_POINT('Origin',(0.,0.375,0.));
#17086=CARTESIAN_POINT('',(-0.35,0.35,-4.28626379701573E-17));
#17087=CARTESIAN_POINT('Origin',(0.,0.35,0.));
#17088=CARTESIAN_POINT('',(-0.325,0.375,-3.9801020972289E-17));
#17089=CARTESIAN_POINT('Origin',(0.,0.19,0.));
#17090=CARTESIAN_POINT('',(-0.35,0.03,-4.28626379701574E-17));
#17091=CARTESIAN_POINT('Origin',(0.,0.03,0.));
#17092=CARTESIAN_POINT('',(-0.35,0.19,-4.28626379701574E-17));
#17093=CARTESIAN_POINT('Origin',(0.,0.0149999999999999,0.));
#17094=CARTESIAN_POINT('',(-0.32,-3.29597460435593E-17,-3.91886975727153E-17));
#17095=CARTESIAN_POINT('Origin',(0.,0.,0.));
#17096=CARTESIAN_POINT('',(-0.335,0.0149999999999999,-4.10256677714363E-17));
#17097=CARTESIAN_POINT('Origin',(0.22,0.,0.));
#17098=CARTESIAN_POINT('',(-0.22,-6.93889390390723E-18,-2.69422295812418E-17));
#17099=CARTESIAN_POINT('Origin',(0.,0.,0.));
#17100=CARTESIAN_POINT('Origin',(0.,-0.02,0.));
#17101=CARTESIAN_POINT('',(-0.1954,-0.0492,2.39295984553393E-17));
#17102=CARTESIAN_POINT('Origin',(0.,-0.0492,0.));
#17103=CARTESIAN_POINT('',(-0.21,-0.02,-2.57175827820944E-17));
#17104=CARTESIAN_POINT('Origin',(0.,-0.8,0.));
#17105=CARTESIAN_POINT('',(-0.1954,-0.8,-2.39295984553393E-17));
#17260=UNCERTAINTY_MEASURE_WITH_UNIT(LENGTH_MEASURE(0.001),#17323,
'DISTANCE_ACCURACY_VALUE',
'Maximum model space distance between geometric entities at asserted c
onnectivities');
#17261=UNCERTAINTY_MEASURE_WITH_UNIT(LENGTH_MEASURE(0.001),#17323,
'DISTANCE_ACCURACY_VALUE',
'Maximum model space distance between geometric entities at asserted c
onnectivities');
#17321=(
GEOMETRIC_REPRESENTATION_CONTEXT(3)
GLOBAL_UNCERTAINTY_ASSIGNED_CONTEXT((#17260))
GLOBAL_UNIT_ASSIGNED_CONTEXT((#17323,#17325,#17326))
REPRESENTATION_CONTEXT('','3D')
);
#17322=(
GEOMETRIC_REPRESENTATION_CONTEXT(3)
GLOBAL_UNCERTAINTY_ASSIGNED_CONTEXT((#17261))
GLOBAL_UNIT_ASSIGNED_CONTEXT((#17323,#17325,#17326))
REPRESENTATION_CONTEXT('','3D')
);
#17323=(
LENGTH_UNIT()
NAMED_UNIT(*)
SI_UNIT(.CENTI.,.METRE.)
);
#17325=(
NAMED_UNIT(*)
PLANE_ANGLE_UNIT()
SI_UNIT($,.RADIAN.)
);
#17326=(
NAMED_UNIT(*)
SI_UNIT($,.STERADIAN.)
SOLID_ANGLE_UNIT()
);
#17386=SHAPE_DEFINITION_REPRESENTATION(#17462,#17617);
#17462=PRODUCT_DEFINITION_SHAPE('',$,#17678);
#17617=SHAPE_REPRESENTATION('',(#10711),#17321);
#17618=PRODUCT_DEFINITION_CONTEXT('part definition',#17800,'design');
#17678=PRODUCT_DEFINITION('M4x10 Cap Screw','M4x10 Cap Screw',#17738,#17618);
#17738=PRODUCT_DEFINITION_FORMATION('',$,#17861);
#17800=APPLICATION_CONTEXT(
'Core Data for Automotive Mechanical Design Process');
#17801=PRODUCT_CONTEXT('part definition',#17800,'mechanical');
#17861=PRODUCT('M4x10 Cap Screw','M4x10 Cap Screw','M4x10 Cap Screw',(#17801));
#17932=COLOUR_RGB('Black',0.12,0.14,0.17);
#17933=FILL_AREA_STYLE_COLOUR('',#17932);
#17934=FILL_AREA_STYLE('',(#17933));
#17935=SURFACE_STYLE_FILL_AREA(#17934);
#17936=SURFACE_SIDE_STYLE('',(#17935));
#17937=SURFACE_STYLE_USAGE(.BOTH.,#17936);
#17938=PRESENTATION_STYLE_ASSIGNMENT((#17937));
ENDSEC;
END-ISO-10303-21;
